ISO-10303-21;
HEADER;
/* Generated by software containing ST-Developer
 * from STEP Tools, Inc. (www.steptools.com) 
 */

FILE_DESCRIPTION(
/* description */ ('Hand-crank flanged shaft unit'),
/* implementation_level */ '2;1');

FILE_NAME(
/* name */ 'Flange bolt sleeve (3).step',
/* time_stamp */ '2026-10-27T18:35:45-07:00',
/* author */ (''),
/* organization */ (''),
/* preprocessor_version */ 'ST-DEVELOPER v20.2',
/* originating_system */ 'Autodesk Translation Framework v15.17.0.0',
/* authorisation */ '');

FILE_SCHEMA (('AUTOMOTIVE_DESIGN { 1 0 10303 214 3 1 1 }'));
ENDSEC;

DATA;
#10=MECHANICAL_DESIGN_GEOMETRIC_PRESENTATION_REPRESENTATION('',(#283),#6805);
#243=SHAPE_REPRESENTATION_RELATIONSHIP('SRR','None',#6904,#263);
#263=ADVANCED_BREP_SHAPE_REPRESENTATION('',(#304),#6787);
#283=STYLED_ITEM('',(#7098),#304);
#304=MANIFOLD_SOLID_BREP('Body1',#3324);
#348=FACE_BOUND('',#772,.T.);
#349=FACE_BOUND('',#774,.T.);
#432=PLANE('',#3635);
#433=PLANE('',#3636);
#553=FACE_OUTER_BOUND('',#769,.T.);
#554=FACE_OUTER_BOUND('',#770,.T.);
#555=FACE_OUTER_BOUND('',#771,.T.);
#556=FACE_OUTER_BOUND('',#773,.T.);
#769=EDGE_LOOP('',(#2419,#2420,#2421,#2422));
#770=EDGE_LOOP('',(#2423,#2424,#2425,#2426));
#771=EDGE_LOOP('',(#2427));
#772=EDGE_LOOP('',(#2428));
#773=EDGE_LOOP('',(#2429));
#774=EDGE_LOOP('',(#2430));
#1033=LINE('',#5121,#1261);
#1034=LINE('',#5127,#1262);
#1261=VECTOR('',#4146,0.425);
#1262=VECTOR('',#4153,0.595);
#1469=CIRCLE('',#3630,0.425);
#1470=CIRCLE('',#3631,0.425);
#1471=CIRCLE('',#3633,0.595);
#1472=CIRCLE('',#3634,0.595);
#1625=VERTEX_POINT('',#5118);
#1626=VERTEX_POINT('',#5120);
#1627=VERTEX_POINT('',#5124);
#1628=VERTEX_POINT('',#5126);
#1927=EDGE_CURVE('',#1625,#1625,#1469,.T.);
#1928=EDGE_CURVE('',#1625,#1626,#1033,.T.);
#1929=EDGE_CURVE('',#1626,#1626,#1470,.T.);
#1930=EDGE_CURVE('',#1627,#1627,#1471,.T.);
#1931=EDGE_CURVE('',#1627,#1628,#1034,.T.);
#1932=EDGE_CURVE('',#1628,#1628,#1472,.T.);
#2419=ORIENTED_EDGE('',*,*,#1927,.F.);
#2420=ORIENTED_EDGE('',*,*,#1928,.T.);
#2421=ORIENTED_EDGE('',*,*,#1929,.T.);
#2422=ORIENTED_EDGE('',*,*,#1928,.F.);
#2423=ORIENTED_EDGE('',*,*,#1930,.F.);
#2424=ORIENTED_EDGE('',*,*,#1931,.T.);
#2425=ORIENTED_EDGE('',*,*,#1932,.T.);
#2426=ORIENTED_EDGE('',*,*,#1931,.F.);
#2427=ORIENTED_EDGE('',*,*,#1930,.T.);
#2428=ORIENTED_EDGE('',*,*,#1927,.T.);
#2429=ORIENTED_EDGE('',*,*,#1932,.F.);
#2430=ORIENTED_EDGE('',*,*,#1929,.F.);
#3083=CYLINDRICAL_SURFACE('',#3629,0.425);
#3084=CYLINDRICAL_SURFACE('',#3632,0.595);
#3170=ADVANCED_FACE('',(#553),#3083,.F.);
#3171=ADVANCED_FACE('',(#554),#3084,.T.);
#3172=ADVANCED_FACE('',(#555,#348),#432,.T.);
#3173=ADVANCED_FACE('',(#556,#349),#433,.F.);
#3324=CLOSED_SHELL('',(#3170,#3171,#3172,#3173));
#3628=AXIS2_PLACEMENT_3D('',#5116,#4140,#4141);
#3629=AXIS2_PLACEMENT_3D('',#5117,#4142,#4143);
#3630=AXIS2_PLACEMENT_3D('',#5119,#4144,#4145);
#3631=AXIS2_PLACEMENT_3D('',#5122,#4147,#4148);
#3632=AXIS2_PLACEMENT_3D('',#5123,#4149,#4150);
#3633=AXIS2_PLACEMENT_3D('',#5125,#4151,#4152);
#3634=AXIS2_PLACEMENT_3D('',#5128,#4154,#4155);
#3635=AXIS2_PLACEMENT_3D('',#5129,#4156,#4157);
#3636=AXIS2_PLACEMENT_3D('',#5130,#4158,#4159);
#4140=DIRECTION('axis',(0.,0.,1.));
#4141=DIRECTION('refdir',(1.,0.,0.));
#4142=DIRECTION('center_axis',(0.,1.,0.));
#4143=DIRECTION('ref_axis',(1.,0.,0.));
#4144=DIRECTION('center_axis',(0.,-1.,0.));
#4145=DIRECTION('ref_axis',(1.,0.,0.));
#4146=DIRECTION('',(0.,-1.,0.));
#4147=DIRECTION('center_axis',(0.,-1.,0.));
#4148=DIRECTION('ref_axis',(1.,0.,0.));
#4149=DIRECTION('center_axis',(0.,1.,0.));
#4150=DIRECTION('ref_axis',(1.,0.,0.));
#4151=DIRECTION('center_axis',(0.,1.,0.));
#4152=DIRECTION('ref_axis',(1.,0.,0.));
#4153=DIRECTION('',(0.,-1.,0.));
#4154=DIRECTION('center_axis',(0.,1.,0.));
#4155=DIRECTION('ref_axis',(1.,0.,0.));
#4156=DIRECTION('center_axis',(0.,1.,0.));
#4157=DIRECTION('ref_axis',(1.,0.,0.));
#4158=DIRECTION('center_axis',(0.,1.,0.));
#4159=DIRECTION('ref_axis',(1.,0.,0.));
#5116=CARTESIAN_POINT('',(0.,0.,0.));
#5117=CARTESIAN_POINT('Origin',(3.2,-1.,10.7));
#5118=CARTESIAN_POINT('',(2.775,0.,10.7));
#5119=CARTESIAN_POINT('Origin',(3.2,0.,10.7));
#5120=CARTESIAN_POINT('',(2.775,-1.,10.7));
#5121=CARTESIAN_POINT('',(2.775,-1.,10.7));
#5122=CARTESIAN_POINT('Origin',(3.2,-1.,10.7));
#5123=CARTESIAN_POINT('Origin',(3.2,-1.,10.7));
#5124=CARTESIAN_POINT('',(2.605,0.,10.7));
#5125=CARTESIAN_POINT('Origin',(3.2,0.,10.7));
#5126=CARTESIAN_POINT('',(2.605,-1.,10.7));
#5127=CARTESIAN_POINT('',(2.605,-1.,10.7));
#5128=CARTESIAN_POINT('Origin',(3.2,-1.,10.7));
#5129=CARTESIAN_POINT('Origin',(3.2,0.,10.7));
#5130=CARTESIAN_POINT('Origin',(3.2,-1.,10.7));
#6762=UNCERTAINTY_MEASURE_WITH_UNIT(LENGTH_MEASURE(0.001),#6806,
'DISTANCE_ACCURACY_VALUE',
'Maximum model space distance between geometric entities at asserted c
onnectivities');
#6780=UNCERTAINTY_MEASURE_WITH_UNIT(LENGTH_MEASURE(0.001),#6806,
'DISTANCE_ACCURACY_VALUE',
'Maximum model space distance between geometric entities at asserted c
onnectivities');
#6787=(
GEOMETRIC_REPRESENTATION_CONTEXT(3)
GLOBAL_UNCERTAINTY_ASSIGNED_CONTEXT((#6762))
GLOBAL_UNIT_ASSIGNED_CONTEXT((#6806,#6808,#6809))
REPRESENTATION_CONTEXT('','3D')
);
#6805=(
GEOMETRIC_REPRESENTATION_CONTEXT(3)
GLOBAL_UNCERTAINTY_ASSIGNED_CONTEXT((#6780))
GLOBAL_UNIT_ASSIGNED_CONTEXT((#6806,#6808,#6809))
REPRESENTATION_CONTEXT('','3D')
);
#6806=(
LENGTH_UNIT()
NAMED_UNIT(*)
SI_UNIT(.CENTI.,.METRE.)
);
#6808=(
NAMED_UNIT(*)
PLANE_ANGLE_UNIT()
SI_UNIT($,.RADIAN.)
);
#6809=(
NAMED_UNIT(*)
SI_UNIT($,.STERADIAN.)
SOLID_ANGLE_UNIT()
);
#6816=SHAPE_DEFINITION_REPRESENTATION(#6840,#6904);
#6840=PRODUCT_DEFINITION_SHAPE('',$,#6929);
#6904=SHAPE_REPRESENTATION('',(#3628),#6787);
#6922=PRODUCT_DEFINITION_CONTEXT('part definition',#6996,'design');
#6929=PRODUCT_DEFINITION('Flange bolt sleeve (3)',
'Flange bolt sleeve (3)',#6953,#6922);
#6953=PRODUCT_DEFINITION_FORMATION('',$,#7004);
#6996=APPLICATION_CONTEXT(
'Core Data for Automotive Mechanical Design Process');
#6997=PRODUCT_CONTEXT('part definition',#6996,'mechanical');
#7004=PRODUCT('Flange bolt sleeve (3)','Flange bolt sleeve (3)',
'Flange bolt sleeve (3)',(#6997));
#7092=COLOUR_RGB('Black',0.12,0.14,0.17);
#7093=FILL_AREA_STYLE_COLOUR('',#7092);
#7094=FILL_AREA_STYLE('',(#7093));
#7095=SURFACE_STYLE_FILL_AREA(#7094);
#7096=SURFACE_SIDE_STYLE('',(#7095));
#7097=SURFACE_STYLE_USAGE(.BOTH.,#7096);
#7098=PRESENTATION_STYLE_ASSIGNMENT((#7097));
ENDSEC;
END-ISO-10303-21;
